ISO-10303-21;
HEADER;
FILE_DESCRIPTION (('STEP AP214'),
    '1' );
FILE_NAME ('socket head cap screw_iso_ISO 4762 M8 x 12 - 12N.step',
    '2026-10-25T16:39:07',
    ( '' ),
    ( '' ),
    'SwSTEP 2.0',
    'SolidWorks 2026',
    '' );
FILE_SCHEMA (( 'AUTOMOTIVE_DESIGN' ));
ENDSEC;

DATA;
#3=EDGE_LOOP ( 'NONE', ( #1646, #9949, #917, #16022, #4902 ) ) ;
#26=CYLINDRICAL_SURFACE ( 'NONE', #5055, 6.500000000000000000 ) ;
#32=DIRECTION ( 'NONE',  ( 1.000000000000000000, 0.000000000000000000, 0.000000000000000000 ) ) ;
#43=FACE_OUTER_BOUND ( 'NONE', #17351, .T. ) ;
#44=LINE ( 'NONE', #5782, #7268 ) ;
#76=( GEOMETRIC_REPRESENTATION_CONTEXT ( 3 ) GLOBAL_UNCERTAINTY_ASSIGNED_CONTEXT ( ( #9698 ) ) GLOBAL_UNIT_ASSIGNED_CONTEXT ( ( #9720, #5466, #12594 ) ) REPRESENTATION_CONTEXT ( 'NONE', 'WORKASPACE' ) );
#130=DIRECTION ( 'NONE',  ( -1.000000000000000000, 0.000000000000000000, -0.000000000000000000 ) ) ;
#155=PRODUCT_DEFINITION ( 'UNKNOWN', '', #10424, #5149 ) ;
#190=ORIENTED_EDGE ( 'NONE', *, *, #1172, .T. ) ;
#192=CARTESIAN_POINT ( 'NONE',  ( 4.000000000000000000, 3.518949890710770134, -4.119968255444916849E-15 ) ) ;
#250=ORIENTED_EDGE ( 'NONE', *, *, #10800, .T. ) ;
#270=CARTESIAN_POINT ( 'NONE',  ( 8.399999999999998579, 5.388445916248356971E-16, 4.400000000000002132 ) ) ;
#273=AXIS2_PLACEMENT_3D ( 'NONE', #9056, #14733, #2489 ) ;
#302=AXIS2_PLACEMENT_3D ( 'NONE', #7360, #4404, #10044 ) ;
#374=ORIENTED_EDGE ( 'NONE', *, *, #3443, .F. ) ;
#376=AXIS2_PLACEMENT_3D ( 'NONE', #11944, #14654, #7580 ) ;
#390=PLANE ( 'NONE',  #7793 ) ;
#391=AXIS2_PLACEMENT_3D ( 'NONE', #10919, #2589, #8131 ) ;
#393=ORIENTED_EDGE ( 'NONE', *, *, #5115, .F. ) ;
#411=LINE ( 'NONE', #3377, #16857 ) ;
#442=ORIENTED_EDGE ( 'NONE', *, *, #6706, .F. ) ;
#483=EDGE_CURVE ( 'NONE', #4093, #15831, #6358, .T. ) ;
#513=FACE_OUTER_BOUND ( 'NONE', #11617, .T. ) ;
#516=CIRCLE ( 'NONE', #8483, 4.400000000000002132 ) ;
#526=VERTEX_POINT ( 'NONE', #13484 ) ;
#552=EDGE_LOOP ( 'NONE', ( #5619, #2064, #7284, #8498 ) ) ;
#568=DIRECTION ( 'NONE',  ( 0.000000000000000000, -1.000000000000000000, 0.000000000000000000 ) ) ;
#575=CIRCLE ( 'NONE', #9148, 0.4000000000000001887 ) ;
#599=CARTESIAN_POINT ( 'NONE',  ( -31.74999999999995737, 0.000000000000000000, 0.000000000000000000 ) ) ;
#617=CARTESIAN_POINT ( 'NONE',  ( -31.74999999999995737, 0.000000000000000000, 0.000000000000000000 ) ) ;
#660=EDGE_CURVE ( 'NONE', #8755, #15831, #10339, .T. ) ;
#664=EDGE_CURVE ( 'NONE', #15831, #13916, #15675, .T. ) ;
#681=( GEOMETRIC_REPRESENTATION_CONTEXT ( 3 ) GLOBAL_UNCERTAINTY_ASSIGNED_CONTEXT ( ( #15795 ) ) GLOBAL_UNIT_ASSIGNED_CONTEXT ( ( #11823, #4782, #14341 ) ) REPRESENTATION_CONTEXT ( 'NONE', 'WORKASPACE' ) );
#699=DIRECTION ( 'NONE',  ( 1.000000000000000000, 0.000000000000000000, 0.000000000000000000 ) ) ;
#708=ORIENTED_EDGE ( 'NONE', *, *, #8626, .T. ) ;
#752=DIRECTION ( 'NONE',  ( 0.000000000000000000, -1.000000000000000000, 0.000000000000000000 ) ) ;
#759=CARTESIAN_POINT ( 'NONE',  ( 0.3999999999999975797, 0.000000000000000000, 0.000000000000000000 ) ) ;
#879=AXIS2_PLACEMENT_3D ( 'NONE', #12311, #1109, #2418 ) ;
#906=DIRECTION ( 'NONE',  ( 0.000000000000000000, 0.8660254037844380415, -0.5000000000000011102 ) ) ;
#917=ORIENTED_EDGE ( 'NONE', *, *, #11339, .T. ) ;
#928=DIRECTION ( 'NONE',  ( -1.000000000000000000, -0.000000000000000000, -0.000000000000000000 ) ) ;
#966=LINE ( 'NONE', #2454, #5685 ) ;
#1002=AXIS2_PLACEMENT_3D ( 'NONE', #4784, #16114, #17423 ) ;
#1014=DIRECTION ( 'NONE',  ( 0.000000000000000000, 0.4999999999999990008, -0.8660254037844391517 ) ) ;
#1029=CARTESIAN_POINT ( 'NONE',  ( 4.000000000000000000, -1.759474945355388176, -3.047499999999998099 ) ) ;
#1080=FACE_OUTER_BOUND ( 'NONE', #10617, .T. ) ;
#1102=AXIS2_PLACEMENT_3D ( 'NONE', #5132, #6527, #3742 ) ;
#1109=DIRECTION ( 'NONE',  ( 1.000000000000000000, 0.000000000000000000, 0.000000000000000000 ) ) ;
#1138=DIRECTION ( 'NONE',  ( 0.000000000000000000, 0.000000000000000000, -1.000000000000000000 ) ) ;
#1172=EDGE_CURVE ( 'NONE', #1302, #13373, #966, .T. ) ;
#1186=CYLINDRICAL_SURFACE ( 'NONE', #15336, 4.000000000000001776 ) ;
#1195=CIRCLE ( 'NONE', #14837, 6.500000000000000000 ) ;
#1205=DIRECTION ( 'NONE',  ( -1.000000000000000000, -0.000000000000000000, -0.000000000000000000 ) ) ;
#1233=VECTOR ( 'NONE', #10797, 1000.000000000000000 ) ;
#1291=ORIENTED_EDGE ( 'NONE', *, *, #4095, .F. ) ;
#1302=VERTEX_POINT ( 'NONE', #5762 ) ;
#1323=PLANE ( 'NONE',  #6525 ) ;
#1326=VERTEX_POINT ( 'NONE', #5669 ) ;
#1385=LINE ( 'NONE', #4248, #11708 ) ;
#1533=FACE_BOUND ( 'NONE', #8591, .T. ) ;
#1597=ORIENTED_EDGE ( 'NONE', *, *, #4750, .T. ) ;
#1603=DIRECTION ( 'NONE',  ( -1.000000000000000000, -0.000000000000000000, -0.000000000000000000 ) ) ;
#1607=EDGE_CURVE ( 'NONE', #7588, #10009, #9632, .T. ) ;
#1615=ORIENTED_EDGE ( 'NONE', *, *, #2991, .F. ) ;
#1642=MANIFOLD_SOLID_BREP ( 'Hex', #18027 ) ;
#1643=EDGE_LOOP ( 'NONE', ( #15088, #14719, #5176 ) ) ;
#1646=ORIENTED_EDGE ( 'NONE', *, *, #1172, .F. ) ;
#1678=VECTOR ( 'NONE', #12083, 1000.000000000000000 ) ;
#1705=FACE_OUTER_BOUND ( 'NONE', #17283, .T. ) ;
#1753=DIRECTION ( 'NONE',  ( 0.000000000000000000, -0.5000000000000011102, -0.8660254037844380415 ) ) ;
#1773=EDGE_LOOP ( 'NONE', ( #15553, #2723 ) ) ;
#1785=FACE_OUTER_BOUND ( 'NONE', #17905, .T. ) ;
#1804=DIRECTION ( 'NONE',  ( 0.000000000000000000, 0.000000000000000000, 1.000000000000000000 ) ) ;
#1810=LINE ( 'NONE', #4763, #17017 ) ;
#1851=STYLED_ITEM('',(#18417),#1642);
#1858=MECHANICAL_DESIGN_GEOMETRIC_PRESENTATION_REPRESENTATION('',(#2153),#681);
#1876=CARTESIAN_POINT ( 'NONE',  ( 4.000000000000000000, 1.759474945355381514, -3.047500000000001652 ) ) ;
#1912=FACE_OUTER_BOUND ( 'NONE', #18168, .T. ) ;
#1976=ORIENTED_EDGE ( 'NONE', *, *, #5479, .T. ) ;
#2002=DIRECTION ( 'NONE',  ( 0.000000000000000000, -0.8660254037844390407, -0.4999999999999993339 ) ) ;
#2043=EDGE_LOOP ( 'NONE', ( #15478, #17092, #6732, #11472 ) ) ;
#2064=ORIENTED_EDGE ( 'NONE', *, *, #16585, .F. ) ;
#2116=VECTOR ( 'NONE', #10912, 1000.000000000000000 ) ;
#2146=LINE ( 'NONE', #7777, #15092 ) ;
#2153=STYLED_ITEM ( 'NONE', ( #16017 ), #12694 ) ;
#2201=AXIS2_PLACEMENT_3D ( 'NONE', #11615, #4484, #11424 ) ;
#2233=ORIENTED_EDGE ( 'NONE', *, *, #12940, .T. ) ;
#2308=CARTESIAN_POINT ( 'NONE',  ( 8.000000000000000000, 7.960204194457795477E-16, -6.500000000000000000 ) ) ;
#2317=ADVANCED_FACE ( 'NONE', ( #13074 ), #12223, .T. ) ;
#2322=ADVANCED_FACE ( 'NONE', ( #1785 ), #390, .F. ) ;
#2352=ORIENTED_EDGE ( 'NONE', *, *, #3438, .F. ) ;
#2418=DIRECTION ( 'NONE',  ( 0.000000000000000000, 0.000000000000000000, -1.000000000000000000 ) ) ;
#2454=CARTESIAN_POINT ( 'NONE',  ( 4.000000000000000000, 3.732111120401558708E-16, -3.047499999999999876 ) ) ;
#2489=DIRECTION ( 'NONE',  ( 0.000000000000000000, 0.000000000000000000, -1.000000000000000000 ) ) ;
#2520=CARTESIAN_POINT ( 'NONE',  ( 0.3999999999999975797, 0.000000000000000000, 0.000000000000000000 ) ) ;
#2522=ORIENTED_EDGE ( 'NONE', *, *, #12871, .T. ) ;
#2538=ORIENTED_EDGE ( 'NONE', *, *, #9374, .F. ) ;
#2579=DIRECTION ( 'NONE',  ( -1.000000000000000000, -0.000000000000000000, -0.000000000000000000 ) ) ;
#2589=DIRECTION ( 'NONE',  ( -1.000000000000000000, -0.000000000000000000, -0.000000000000000000 ) ) ;
#2609=CARTESIAN_POINT ( 'NONE',  ( 0.000000000000000000, -1.759474945355381292, 3.047500000000002540 ) ) ;
#2629=AXIS2_PLACEMENT_3D ( 'NONE', #10208, #14504, #12903 ) ;
#2691=PLANE ( 'NONE',  #15696 ) ;
#2693=CARTESIAN_POINT ( 'NONE',  ( 4.000000000000000000, -2.639212418033078489, -1.523749999999996829 ) ) ;
#2723=ORIENTED_EDGE ( 'NONE', *, *, #6265, .T. ) ;
#2749=ADVANCED_FACE ( 'NONE', ( #513 ), #10094, .F. ) ;
#2757=CARTESIAN_POINT ( 'NONE',  ( 0.000000000000000000, 0.000000000000000000, 6.099999999999999645 ) ) ;
#2763=AXIS2_PLACEMENT_3D ( 'NONE', #16571, #14992, #8293 ) ;
#2779=CIRCLE ( 'NONE', #8093, 6.099999999999999645 ) ;
#2857=CARTESIAN_POINT ( 'NONE',  ( 4.000000000000000000, 3.518949890710770134, -4.119968255444916849E-15 ) ) ;
#2929=AXIS2_PLACEMENT_3D ( 'NONE', #10720, #906, #6548 ) ;
#2941=VECTOR ( 'NONE', #8945, 1000.000000000000114 ) ;
#2944=ORIENTED_EDGE ( 'NONE', *, *, #664, .F. ) ;
#2960=ORIENTED_EDGE ( 'NONE', *, *, #3438, .T. ) ;
#2991=EDGE_CURVE ( 'NONE', #4808, #13964, #11297, .T. ) ;
#3046=AXIS2_PLACEMENT_3D ( 'NONE', #6032, #14041, #11684 ) ;
#3069=CARTESIAN_POINT ( 'NONE',  ( 4.000000000000000000, 3.518949890710770134, -4.119968255444916849E-15 ) ) ;
#3071=ORIENTED_EDGE ( 'NONE', *, *, #11068, .T. ) ;
#3092=EDGE_CURVE ( 'NONE', #10922, #526, #18147, .T. ) ;
#3130=VERTEX_POINT ( 'NONE', #1029 ) ;
#3195=DIRECTION ( 'NONE',  ( 0.000000000000000000, 0.000000000000000000, -1.000000000000000000 ) ) ;
#3228=CARTESIAN_POINT ( 'NONE',  ( 0.000000000000000000, 3.518949890710770134, -4.119968255444916849E-15 ) ) ;
#3328=EDGE_CURVE ( 'NONE', #16052, #14634, #10434, .T. ) ;
#3348=CARTESIAN_POINT ( 'NONE',  ( 8.399999999999998579, 0.000000000000000000, -4.400000000000002132 ) ) ;
#3377=CARTESIAN_POINT ( 'NONE',  ( 20.00000000000000355, 0.000000000000000000, 3.309499999999999886 ) ) ;
#3403=CARTESIAN_POINT ( 'NONE',  ( 20.00000000000000000, 3.309499999999999886, 0.000000000000000000 ) ) ;
#3404=FILL_AREA_STYLE ('',( #10149 ) ) ;
#3413=PLANE ( 'NONE',  #273 ) ;
#3438=EDGE_CURVE ( 'NONE', #7494, #16052, #12801, .T. ) ;
#3443=EDGE_CURVE ( 'NONE', #1302, #13916, #4896, .T. ) ;
#3444=DIRECTION ( 'NONE',  ( -1.000000000000000000, -0.000000000000000000, -0.000000000000000000 ) ) ;
#3463=CARTESIAN_POINT ( 'NONE',  ( 4.000000000000000000, -3.518949890710769246, 4.119968255444916849E-15 ) ) ;
#3469=DIRECTION ( 'NONE',  ( -1.000000000000000000, -0.000000000000000000, -0.000000000000000000 ) ) ;
#3492=CARTESIAN_POINT ( 'NONE',  ( 4.000000000000000000, 1.759474945355387954, 3.047499999999997211 ) ) ;
#3508=LINE ( 'NONE', #14547, #14137 ) ;
#3526=DIRECTION ( 'NONE',  ( 0.000000000000000000, 0.000000000000000000, -1.000000000000000000 ) ) ;
#3539=DIRECTION ( 'NONE',  ( 0.000000000000000000, -9.859324684083080328E-16, -1.000000000000000000 ) ) ;
#3557=ORIENTED_EDGE ( 'NONE', *, *, #12833, .T. ) ;
#3562=ORIENTED_EDGE ( 'NONE', *, *, #4707, .F. ) ;
#3613=DIRECTION ( 'NONE',  ( 0.000000000000000000, -0.4999999999999992784, 0.8660254037844389297 ) ) ;
#3621=ORIENTED_EDGE ( 'NONE', *, *, #9034, .F. ) ;
#3643=LINE ( 'NONE', #9015, #16917 ) ;
#3692=ORIENTED_EDGE ( 'NONE', *, *, #3328, .F. ) ;
#3739=AXIS2_PLACEMENT_3D ( 'NONE', #13593, #12017, #6372 ) ;
#3742=DIRECTION ( 'NONE',  ( 0.000000000000000000, -1.224646799147353207E-16, 1.000000000000000000 ) ) ;
#3757=SHAPE_DEFINITION_REPRESENTATION ( #9300, #10770 ) ;
#3768=FACE_OUTER_BOUND ( 'NONE', #4722, .T. ) ;
#3808=VERTEX_POINT ( 'NONE', #15827 ) ;
#3821=DIRECTION ( 'NONE',  ( -1.000000000000000000, -0.000000000000000000, -0.000000000000000000 ) ) ;
#3885=DIRECTION ( 'NONE',  ( -1.000000000000000000, -0.000000000000000000, -0.000000000000000000 ) ) ;
#3916=AXIS2_PLACEMENT_3D ( 'NONE', #192, #17006, #5842 ) ;
#3923=( GEOMETRIC_REPRESENTATION_CONTEXT ( 3 ) GLOBAL_UNCERTAINTY_ASSIGNED_CONTEXT ( ( #10851 ) ) GLOBAL_UNIT_ASSIGNED_CONTEXT ( ( #8221, #13885, #5444 ) ) REPRESENTATION_CONTEXT ( 'NONE', 'WORKASPACE' ) );
#3936=CARTESIAN_POINT ( 'NONE',  ( 4.000000000000000000, 0.000000000000000000, 0.000000000000000000 ) ) ;
#3953=ADVANCED_FACE ( 'NONE', ( #13402 ), #13488, .T. ) ;
#3964=CARTESIAN_POINT ( 'NONE',  ( 0.000000000000000000, 0.000000000000000000, 0.000000000000000000 ) ) ;
#4024=VECTOR ( 'NONE', #1603, 1000.000000000000000 ) ;
#4050=ORIENTED_EDGE ( 'NONE', *, *, #8689, .T. ) ;
#4086=DIRECTION ( 'NONE',  ( 0.000000000000000000, -0.4999999999999990563, 0.8660254037844391517 ) ) ;
#4092=AXIS2_PLACEMENT_3D ( 'NONE', #8633, #15701, #13093 ) ;
#4093=VERTEX_POINT ( 'NONE', #6450 ) ;
#4095=EDGE_CURVE ( 'NONE', #10626, #13628, #16694, .T. ) ;
#4148=DIRECTION ( 'NONE',  ( -1.000000000000000000, -0.000000000000000000, -0.000000000000000000 ) ) ;
#4185=ADVANCED_FACE ( 'NONE', ( #1080 ), #16665, .F. ) ;
#4248=CARTESIAN_POINT ( 'NONE',  ( 4.000000000000000000, -1.759474945355381292, 3.047500000000002540 ) ) ;
#4253=VERTEX_POINT ( 'NONE', #15974 ) ;
#4300=FACE_OUTER_BOUND ( 'NONE', #6390, .T. ) ;
#4332=LINE ( 'NONE', #12338, #4350 ) ;
#4350=VECTOR ( 'NONE', #9979, 1000.000000000000000 ) ;
#4392=LINE ( 'NONE', #14322, #9869 ) ;
#4404=DIRECTION ( 'NONE',  ( -1.000000000000000000, -0.000000000000000000, -0.000000000000000000 ) ) ;
#4435=DIRECTION ( 'NONE',  ( 0.000000000000000000, 1.224646799147353207E-16, 1.000000000000000000 ) ) ;
#4484=DIRECTION ( 'NONE',  ( -1.000000000000000000, -0.000000000000000000, -0.000000000000000000 ) ) ;
#4503=ORIENTED_EDGE ( 'NONE', *, *, #16967, .F. ) ;
#4507=MECHANICAL_DESIGN_GEOMETRIC_PRESENTATION_REPRESENTATION('',(#1851),#76);
#4514=DIRECTION ( 'NONE',  ( 1.000000000000000000, 0.000000000000000000, 0.000000000000000000 ) ) ;
#4619=EDGE_CURVE ( 'NONE', #12954, #16052, #8403, .T. ) ;
#4624=EDGE_CURVE ( 'NONE', #12442, #8755, #13702, .T. ) ;
#4656=ORIENTED_EDGE ( 'NONE', *, *, #1607, .T. ) ;
#4674=ADVANCED_FACE ( 'NONE', ( #9432 ), #18177, .F. ) ;
#4707=EDGE_CURVE ( 'NONE', #526, #13373, #13999, .T. ) ;
#4722=EDGE_LOOP ( 'NONE', ( #4050, #7068, #2960, #12915 ) ) ;
#4726=LINE ( 'NONE', #6306, #16419 ) ;
#4739=ORIENTED_EDGE ( 'NONE', *, *, #7940, .T. ) ;
#4750=EDGE_CURVE ( 'NONE', #9690, #10864, #2779, .T. ) ;
#4763=CARTESIAN_POINT ( 'NONE',  ( 4.000000000000000000, 1.759474945355387954, 3.047499999999997211 ) ) ;
#4776=CARTESIAN_POINT ( 'NONE',  ( 4.000000000000000000, -1.759474945355381292, 3.047500000000002540 ) ) ;
#4782=( NAMED_UNIT ( * ) PLANE_ANGLE_UNIT ( ) SI_UNIT ( $, .RADIAN. ) );
#4784=CARTESIAN_POINT ( 'NONE',  ( 20.00000000000000355, 0.000000000000000000, 0.000000000000000000 ) ) ;
#4789=ADVANCED_FACE ( 'NONE', ( #12576 ), #6621, .F. ) ;
#4808=VERTEX_POINT ( 'NONE', #8482 ) ;
#4849=ORIENTED_EDGE ( 'NONE', *, *, #17388, .T. ) ;
#4850=ORIENTED_EDGE ( 'NONE', *, *, #3092, .F. ) ;
#4896=LINE ( 'NONE', #7670, #15763 ) ;
#4902=ORIENTED_EDGE ( 'NONE', *, *, #4707, .T. ) ;
#4970=ORIENTED_EDGE ( 'NONE', *, *, #10207, .T. ) ;
#4987=DIRECTION ( 'NONE',  ( -0.5000000000000061062, 0.000000000000000000, 0.8660254037844351549 ) ) ;
#5005=CARTESIAN_POINT ( 'NONE',  ( 20.00000000000000355, 0.000000000000000000, 0.000000000000000000 ) ) ;
#5025=CARTESIAN_POINT ( 'NONE',  ( 20.00000000000000355, 0.000000000000000000, 3.309499999999999886 ) ) ;
#5047=VERTEX_POINT ( 'NONE', #3492 ) ;
#5055=AXIS2_PLACEMENT_3D ( 'NONE', #14496, #10020, #7239 ) ;
#5064=PLANE ( 'NONE',  #2929 ) ;
#5085=FACE_OUTER_BOUND ( 'NONE', #8902, .T. ) ;
#5115=EDGE_CURVE ( 'NONE', #13628, #10626, #11061, .T. ) ;
#5129=CIRCLE ( 'NONE', #13672, 0.4000000000000001887 ) ;
#5132=CARTESIAN_POINT ( 'NONE',  ( 0.3999999999999975797, 7.470345474798854293E-16, -6.099999999999999645 ) ) ;
#5149=PRODUCT_DEFINITION_CONTEXT ( 'detailed design', #7837, 'design' ) ;
#5176=ORIENTED_EDGE ( 'NONE', *, *, #660, .F. ) ;
#5177=PLANE ( 'NONE',  #6796 ) ;
#5211=ORIENTED_EDGE ( 'NONE', *, *, #7275, .F. ) ;
#5340=DIRECTION ( 'NONE',  ( 0.000000000000000000, -1.000000000000000000, 9.859324684083080328E-16 ) ) ;
#5416=ADVANCED_FACE ( 'NONE', ( #43 ), #6346, .F. ) ;
#5419=DIRECTION ( 'NONE',  ( 0.000000000000000000, 0.000000000000000000, 1.000000000000000000 ) ) ;
#5444=( NAMED_UNIT ( * ) SI_UNIT ( $, .STERADIAN. ) SOLID_ANGLE_UNIT ( ) );
#5466=( NAMED_UNIT ( * ) PLANE_ANGLE_UNIT ( ) SI_UNIT ( $, .RADIAN. ) );
#5476=ADVANCED_FACE ( 'NONE', ( #4300 ), #17904, .T. ) ;
#5479=EDGE_CURVE ( 'NONE', #4093, #7588, #4392, .T. ) ;
#5533=CARTESIAN_POINT ( 'NONE',  ( 4.000000000000000000, 0.000000000000000000, 0.000000000000000000 ) ) ;
#5546=CIRCLE ( 'NONE', #15923, 3.047499999999999876 ) ;
#5578=ADVANCED_FACE ( 'NONE', ( #1912 ), #14705, .F. ) ;
#5595=EDGE_CURVE ( 'NONE', #5047, #4253, #1810, .T. ) ;
#5619=ORIENTED_EDGE ( 'NONE', *, *, #10156, .F. ) ;
#5669=CARTESIAN_POINT ( 'NONE',  ( 0.000000000000000000, -1.759474945355388176, -3.047499999999998099 ) ) ;
#5685=VECTOR ( 'NONE', #10961, 1000.000000000000000 ) ;
#5691=ADVANCED_FACE ( 'NONE', ( #16095 ), #9027, .T. ) ;
#5692=ORIENTED_EDGE ( 'NONE', *, *, #15002, .T. ) ;
#5709=CARTESIAN_POINT ( 'NONE',  ( 8.000000000000000000, 0.000000000000000000, -4.400000000000002132 ) ) ;
#5757=LINE ( 'NONE', #3069, #8836 ) ;
#5762=CARTESIAN_POINT ( 'NONE',  ( 5.759474945355412601, 0.000000000000000000, 0.000000000000000000 ) ) ;
#5772=CARTESIAN_POINT ( 'NONE',  ( 0.3999999999999975797, 0.000000000000000000, 0.000000000000000000 ) ) ;
#5782=CARTESIAN_POINT ( 'NONE',  ( 4.000000000000000000, 3.518949890710770134, -4.119968255444916849E-15 ) ) ;
#5792=DIRECTION ( 'NONE',  ( 0.000000000000000000, 0.000000000000000000, 1.000000000000000000 ) ) ;
#5827=ORIENTED_EDGE ( 'NONE', *, *, #16209, .F. ) ;
#5842=DIRECTION ( 'NONE',  ( 0.000000000000000000, 0.000000000000000000, -1.000000000000000000 ) ) ;
#5872=DIRECTION ( 'NONE',  ( 1.000000000000000000, 0.000000000000000000, 0.000000000000000000 ) ) ;
#5899=EDGE_LOOP ( 'NONE', ( #16314, #6311, #10342, #2522, #8737 ) ) ;
#5955=FACE_OUTER_BOUND ( 'NONE', #2043, .T. ) ;
#5966=AXIS2_PLACEMENT_3D ( 'NONE', #18198, #11109, #13717 ) ;
#5982=DIRECTION ( 'NONE',  ( 0.000000000000000000, 0.000000000000000000, -1.000000000000000000 ) ) ;
#6028=DIRECTION ( 'NONE',  ( 0.000000000000000000, 1.000000000000000000, -9.859324684083080328E-16 ) ) ;
#6032=CARTESIAN_POINT ( 'NONE',  ( 4.000000000000000000, 3.518949890710770134, -4.119968255444916849E-15 ) ) ;
#6045=CARTESIAN_POINT ( 'NONE',  ( 4.000000000000000000, 0.000000000000000000, 0.000000000000000000 ) ) ;
#6118=ORIENTED_EDGE ( 'NONE', *, *, #1607, .F. ) ;
#6202=VECTOR ( 'NONE', #928, 1000.000000000000000 ) ;
#6219=DIRECTION ( 'NONE',  ( -1.000000000000000000, -0.000000000000000000, -0.000000000000000000 ) ) ;
#6255=LINE ( 'NONE', #11908, #8285 ) ;
#6256=DIRECTION ( 'NONE',  ( -1.000000000000000000, -0.000000000000000000, -0.000000000000000000 ) ) ;
#6265=EDGE_CURVE ( 'NONE', #14634, #11376, #17960, .T. ) ;
#6294=EDGE_CURVE ( 'NONE', #16052, #7494, #9054, .T. ) ;
#6306=CARTESIAN_POINT ( 'NONE',  ( 20.00000000000000355, 4.052968581778165278E-16, -3.309499999999999886 ) ) ;
#6311=ORIENTED_EDGE ( 'NONE', *, *, #7424, .F. ) ;
#6346=TOROIDAL_SURFACE ( 'NONE', #15237, 4.400000000000002132, 0.4000000000000000222 ) ;
#6358=LINE ( 'NONE', #4776, #2941 ) ;
#6372=DIRECTION ( 'NONE',  ( 0.000000000000000000, 0.000000000000000000, -1.000000000000000000 ) ) ;
#6390=EDGE_LOOP ( 'NONE', ( #1615, #17715, #10169, #16601 ) ) ;
#6421=ORIENTED_EDGE ( 'NONE', *, *, #5479, .F. ) ;
#6428=DIRECTION ( 'NONE',  ( 1.000000000000000000, 0.000000000000000000, 0.000000000000000000 ) ) ;
#6450=CARTESIAN_POINT ( 'NONE',  ( 4.000000000000000000, -1.759474945355381292, 3.047500000000002540 ) ) ;
#6462=DIRECTION ( 'NONE',  ( 0.000000000000000000, 0.000000000000000000, 1.000000000000000000 ) ) ;
#6469=ORIENTED_EDGE ( 'NONE', *, *, #10045, .T. ) ;
#6475=VECTOR ( 'NONE', #14480, 1000.000000000000227 ) ;
#6525=AXIS2_PLACEMENT_3D ( 'NONE', #11130, #18300, #4086 ) ;
#6527=DIRECTION ( 'NONE',  ( -0.000000000000000000, 1.000000000000000000, 1.224646799147353207E-16 ) ) ;
#6541=ORIENTED_EDGE ( 'NONE', *, *, #5595, .F. ) ;
#6548=DIRECTION ( 'NONE',  ( 0.000000000000000000, 0.5000000000000011102, 0.8660254037844380415 ) ) ;
#6621=CONICAL_SURFACE ( 'NONE', #14624, 3.047499999999999876, 1.047197551196590748 ) ;
#6623=CARTESIAN_POINT ( 'NONE',  ( 4.000000000000000000, -1.759474945355381292, 3.047500000000002540 ) ) ;
#6671=DIRECTION ( 'NONE',  ( 0.000000000000000000, -0.5000000000000011102, -0.8660254037844380415 ) ) ;
#6706=EDGE_CURVE ( 'NONE', #7005, #13964, #12991, .T. ) ;
#6713=ADVANCED_FACE ( 'NONE', ( #12724 ), #26, .T. ) ;
#6732=ORIENTED_EDGE ( 'NONE', *, *, #4619, .T. ) ;
#6738=VERTEX_POINT ( 'NONE', #11500 ) ;
#6748=ORIENTED_EDGE ( 'NONE', *, *, #7500, .T. ) ;
#6763=VECTOR ( 'NONE', #13070, 1000.000000000000000 ) ;
#6792=PRODUCT ( 'socket head cap screw_iso_ISO 4762 M8 x 12 - 12N', 'socket head cap screw_iso_ISO 4762 M8 x 12 - 12N', '', ( #14937 ) ) ;
#6796=AXIS2_PLACEMENT_3D ( 'NONE', #11100, #12222, #7957 ) ;
#6872=CARTESIAN_POINT ( 'NONE',  ( 8.399999999999998579, 0.000000000000000000, 0.000000000000000000 ) ) ;
#6936=ORIENTED_EDGE ( 'NONE', *, *, #8689, .F. ) ;
#6955=DIRECTION ( 'NONE',  ( 0.000000000000000000, -0.4999999999999992784, 0.8660254037844389297 ) ) ;
#6993=CARTESIAN_POINT ( 'NONE',  ( 4.000000000000000000, 0.000000000000000000, 0.000000000000000000 ) ) ;
#7005=VERTEX_POINT ( 'NONE', #12968 ) ;
#7008=ORIENTED_EDGE ( 'NONE', *, *, #17388, .F. ) ;
#7047=DIRECTION ( 'NONE',  ( 1.000000000000000000, 0.000000000000000000, 0.000000000000000000 ) ) ;
#7057=CARTESIAN_POINT ( 'NONE',  ( -31.74999999999995737, 0.000000000000000000, 6.500000000000000000 ) ) ;
#7062=DIRECTION ( 'NONE',  ( -1.000000000000000000, -0.000000000000000000, -0.000000000000000000 ) ) ;
#7068=ORIENTED_EDGE ( 'NONE', *, *, #18139, .T. ) ;
#7074=CARTESIAN_POINT ( 'NONE',  ( 8.399999999999998579, 0.000000000000000000, 0.000000000000000000 ) ) ;
#7086=DIRECTION ( 'NONE',  ( 0.000000000000000000, 0.000000000000000000, 1.000000000000000000 ) ) ;
#7094=EDGE_CURVE ( 'NONE', #13964, #9690, #575, .T. ) ;
#7162=ORIENTED_EDGE ( 'NONE', *, *, #14586, .T. ) ;
#7167=FACE_OUTER_BOUND ( 'NONE', #8417, .T. ) ;
#7168=ORIENTED_EDGE ( 'NONE', *, *, #10045, .F. ) ;
#7204=ORIENTED_EDGE ( 'NONE', *, *, #10999, .T. ) ;
#7231=ORIENTED_EDGE ( 'NONE', *, *, #10999, .F. ) ;
#7236=APPLICATION_CONTEXT ( 'automotive_design' ) ;
#7239=DIRECTION ( 'NONE',  ( 0.000000000000000000, 0.000000000000000000, 1.000000000000000000 ) ) ;
#7248=ORIENTED_EDGE ( 'NONE', *, *, #11882, .T. ) ;
#7252=DIRECTION ( 'NONE',  ( -1.000000000000000000, -0.000000000000000000, -0.000000000000000000 ) ) ;
#7268=VECTOR ( 'NONE', #11425, 1000.000000000000000 ) ;
#7275=EDGE_CURVE ( 'NONE', #3130, #1326, #2146, .T. ) ;
#7284=ORIENTED_EDGE ( 'NONE', *, *, #7094, .T. ) ;
#7306=AXIS2_PLACEMENT_3D ( 'NONE', #5005, #3444, #16153 ) ;
#7339=DIRECTION ( 'NONE',  ( 0.000000000000000000, 0.000000000000000000, 1.000000000000000000 ) ) ;
#7360=CARTESIAN_POINT ( 'NONE',  ( 4.000000000000000000, 0.000000000000000000, 0.000000000000000000 ) ) ;
#7363=ADVANCED_FACE ( 'NONE', ( #8047 ), #5177, .F. ) ;
#7391=ADVANCED_FACE ( 'NONE', ( #15211, #5085 ), #9623, .T. ) ;
#7411=LINE ( 'NONE', #1876, #6763 ) ;
#7418=ORIENTED_EDGE ( 'NONE', *, *, #11882, .F. ) ;
#7424=EDGE_CURVE ( 'NONE', #12442, #10009, #17909, .T. ) ;
#7466=DIRECTION ( 'NONE',  ( 1.000000000000000000, 0.000000000000000000, 0.000000000000000000 ) ) ;
#7494=VERTEX_POINT ( 'NONE', #15299 ) ;
#7500=EDGE_CURVE ( 'NONE', #10864, #9690, #14824, .T. ) ;
#7521=ADVANCED_FACE ( 'NONE', ( #15391 ), #2691, .F. ) ;
#7580=DIRECTION ( 'NONE',  ( 0.000000000000000000, 0.000000000000000000, -1.000000000000000000 ) ) ;
#7588=VERTEX_POINT ( 'NONE', #8489 ) ;
#7619=EDGE_LOOP ( 'NONE', ( #8043, #12753, #6936, #17726 ) ) ;
#7639=CYLINDRICAL_SURFACE ( 'NONE', #16543, 6.500000000000000000 ) ;
#7666=AXIS2_PLACEMENT_3D ( 'NONE', #8289, #8194, #9767 ) ;
#7670=CARTESIAN_POINT ( 'NONE',  ( 4.000000000000000000, 0.000000000000000000, 3.047499999999999876 ) ) ;
#7742=EDGE_LOOP ( 'NONE', ( #10361, #12844, #15825, #17158 ) ) ;
#7752=COLOUR_RGB ( '',1.000000000000000000, 0.9490196078431372140, 0.9098039215686274384 ) ;
#7754=LINE ( 'NONE', #12107, #12993 ) ;
#7777=CARTESIAN_POINT ( 'NONE',  ( 4.000000000000000000, -1.759474945355388176, -3.047499999999998099 ) ) ;
#7779=CARTESIAN_POINT ( 'NONE',  ( 0.000000000000000000, 3.518949890710770134, -4.119968255444916849E-15 ) ) ;
#7792=VERTEX_POINT ( 'NONE', #3228 ) ;
#7793=AXIS2_PLACEMENT_3D ( 'NONE', #16063, #3539, #6028 ) ;
#7824=DIRECTION ( 'NONE',  ( 0.000000000000000000, -0.4999999999999992784, 0.8660254037844389297 ) ) ;
#7837=APPLICATION_CONTEXT ( 'automotive_design' ) ;
#7863=ORIENTED_EDGE ( 'NONE', *, *, #12940, .F. ) ;
#7938=DIRECTION ( 'NONE',  ( 0.000000000000000000, 0.4999999999999990008, -0.8660254037844391517 ) ) ;
#7940=EDGE_CURVE ( 'NONE', #13373, #3130, #10902, .T. ) ;
#7957=DIRECTION ( 'NONE',  ( 0.000000000000000000, 0.000000000000000000, -1.000000000000000000 ) ) ;
#8041=DIRECTION ( 'NONE',  ( -1.000000000000000000, -0.000000000000000000, -0.000000000000000000 ) ) ;
#8043=ORIENTED_EDGE ( 'NONE', *, *, #4095, .T. ) ;
#8047=FACE_OUTER_BOUND ( 'NONE', #17374, .T. ) ;
#8093=AXIS2_PLACEMENT_3D ( 'NONE', #3964, #4148, #9616 ) ;
#8131=DIRECTION ( 'NONE',  ( 0.000000000000000000, 0.000000000000000000, 1.000000000000000000 ) ) ;
#8194=DIRECTION ( 'NONE',  ( -1.000000000000000000, -0.000000000000000000, -0.000000000000000000 ) ) ;
#8221=( LENGTH_UNIT ( ) NAMED_UNIT ( * ) SI_UNIT ( .MILLI., .METRE. ) );
#8284=DIRECTION ( 'NONE',  ( 0.000000000000000000, 1.000000000000000000, -1.478898702612462246E-15 ) ) ;
#8285=VECTOR ( 'NONE', #10608, 1000.000000000000000 ) ;
#8289=CARTESIAN_POINT ( 'NONE',  ( 4.000000000000000000, 0.000000000000000000, 0.000000000000000000 ) ) ;
#8293=DIRECTION ( 'NONE',  ( 0.000000000000000000, 0.000000000000000000, 1.000000000000000000 ) ) ;
#8296=ORIENTED_EDGE ( 'NONE', *, *, #14411, .T. ) ;
#8389=DIRECTION ( 'NONE',  ( -1.000000000000000000, -0.000000000000000000, -0.000000000000000000 ) ) ;
#8403=LINE ( 'NONE', #12397, #8966 ) ;
#8417=EDGE_LOOP ( 'NONE', ( #1597, #6748 ) ) ;
#8463=DIRECTION ( 'NONE',  ( 0.000000000000000000, 0.000000000000000000, -1.000000000000000000 ) ) ;
#8482=CARTESIAN_POINT ( 'NONE',  ( 0.3999999999999975797, 7.960204194457795477E-16, -6.500000000000000000 ) ) ;
#8483=AXIS2_PLACEMENT_3D ( 'NONE', #13829, #14353, #1138 ) ;
#8489=CARTESIAN_POINT ( 'NONE',  ( 0.000000000000000000, -1.759474945355381292, 3.047500000000002540 ) ) ;
#8498=ORIENTED_EDGE ( 'NONE', *, *, #7500, .F. ) ;
#8583=EDGE_CURVE ( 'NONE', #13628, #16136, #4726, .T. ) ;
#8591=EDGE_LOOP ( 'NONE', ( #7162, #4503, #4656, #3071, #5827, #7231 ) ) ;
#8626=EDGE_CURVE ( 'NONE', #7494, #11376, #5129, .T. ) ;
#8633=CARTESIAN_POINT ( 'NONE',  ( 8.000000000000000000, 0.000000000000000000, 0.000000000000000000 ) ) ;
#8684=AXIS2_PLACEMENT_3D ( 'NONE', #16277, #2002, #13295 ) ;
#8689=EDGE_CURVE ( 'NONE', #12954, #16136, #11501, .T. ) ;
#8729=DIRECTION ( 'NONE',  ( 0.000000000000000000, 0.000000000000000000, 1.000000000000000000 ) ) ;
#8737=ORIENTED_EDGE ( 'NONE', *, *, #7275, .T. ) ;
#8750=AXIS2_PLACEMENT_3D ( 'NONE', #18367, #11279, #8769 ) ;
#8755=VERTEX_POINT ( 'NONE', #2693 ) ;
#8769=DIRECTION ( 'NONE',  ( 0.000000000000000000, 0.000000000000000000, 1.000000000000000000 ) ) ;
#8836=VECTOR ( 'NONE', #11580, 999.9999999999998863 ) ;
#8902=EDGE_LOOP ( 'NONE', ( #16516, #3621 ) ) ;
#8919=ORIENTED_EDGE ( 'NONE', *, *, #14586, .F. ) ;
#8945=DIRECTION ( 'NONE',  ( 0.000000000000000000, -0.5000000000000011102, -0.8660254037844380415 ) ) ;
#8951=SURFACE_STYLE_FILL_AREA ( #3404 ) ;
#8956=EDGE_LOOP ( 'NONE', ( #6118, #6421, #17254, #16026, #9135 ) ) ;
#8966=VECTOR ( 'NONE', #8041, 1000.000000000000000 ) ;
#8982=EDGE_CURVE ( 'NONE', #15831, #12442, #1385, .T. ) ;
#8994=DIRECTION ( 'NONE',  ( 0.000000000000000000, 0.000000000000000000, -1.000000000000000000 ) ) ;
#9015=CARTESIAN_POINT ( 'NONE',  ( 0.000000000000000000, -1.759474945355381292, 3.047500000000002540 ) ) ;
#9024=CARTESIAN_POINT ( 'NONE',  ( 0.000000000000000000, 0.000000000000000000, 0.000000000000000000 ) ) ;
#9027=PLANE ( 'NONE',  #8684 ) ;
#9034=EDGE_CURVE ( 'NONE', #17537, #7005, #13195, .T. ) ;
#9037=FACE_OUTER_BOUND ( 'NONE', #12762, .T. ) ;
#9054=CIRCLE ( 'NONE', #16780, 4.000000000000001776 ) ;
#9056=CARTESIAN_POINT ( 'NONE',  ( 4.000000000000000000, 3.518949890710770134, -4.119968255444916849E-15 ) ) ;
#9114=CARTESIAN_POINT ( 'NONE',  ( 4.000000000000000000, 4.506943796211476502E-15, 3.047499999999998987 ) ) ;
#9135=ORIENTED_EDGE ( 'NONE', *, *, #7424, .T. ) ;
#9148=AXIS2_PLACEMENT_3D ( 'NONE', #13248, #568, #3526 ) ;
#9154=DIRECTION ( 'NONE',  ( 0.000000000000000000, -0.5000000000000012212, -0.8660254037844380415 ) ) ;
#9157=LINE ( 'NONE', #13598, #2116 ) ;
#9179=FACE_OUTER_BOUND ( 'NONE', #11891, .T. ) ;
#9300=PRODUCT_DEFINITION_SHAPE ( 'NONE', 'NONE',  #155 ) ;
#9310=LINE ( 'NONE', #10979, #14452 ) ;
#9370=ADVANCED_FACE ( 'NONE', ( #1533, #7167 ), #17311, .T. ) ;
#9374=EDGE_CURVE ( 'NONE', #15136, #7792, #44, .T. ) ;
#9432=FACE_OUTER_BOUND ( 'NONE', #18157, .T. ) ;
#9473=CARTESIAN_POINT ( 'NONE',  ( 8.000000000000000000, 0.000000000000000000, 0.000000000000000000 ) ) ;
#9484=VECTOR ( 'NONE', #6955, 1000.000000000000227 ) ;
#9533=CARTESIAN_POINT ( 'NONE',  ( 8.000000000000000000, 5.388445916248356971E-16, 4.400000000000002132 ) ) ;
#9554=ADVANCED_FACE ( 'NONE', ( #17887 ), #14099, .F. ) ;
#9562=VECTOR ( 'NONE', #1014, 1000.000000000000227 ) ;
#9569=DIRECTION ( 'NONE',  ( 0.000000000000000000, 0.000000000000000000, -1.000000000000000000 ) ) ;
#9586=DIRECTION ( 'NONE',  ( -1.000000000000000000, -0.000000000000000000, -0.000000000000000000 ) ) ;
#9616=DIRECTION ( 'NONE',  ( 0.000000000000000000, 0.000000000000000000, 1.000000000000000000 ) ) ;
#9623=PLANE ( 'NONE',  #879 ) ;
#9632=LINE ( 'NONE', #2609, #17857 ) ;
#9690=VERTEX_POINT ( 'NONE', #2757 ) ;
#9698=UNCERTAINTY_MEASURE_WITH_UNIT (LENGTH_MEASURE( 1.000000000000000082E-05 ), #9720, 'distance_accuracy_value', 'NONE');
#9714=EDGE_LOOP ( 'NONE', ( #10157, #4849, #9833, #442 ) ) ;
#9716=ORIENTED_EDGE ( 'NONE', *, *, #660, .T. ) ;
#9720=( LENGTH_UNIT ( ) NAMED_UNIT ( * ) SI_UNIT ( .MILLI., .METRE. ) );
#9767=DIRECTION ( 'NONE',  ( 0.000000000000000000, 0.000000000000000000, 1.000000000000000000 ) ) ;
#9778=CONICAL_SURFACE ( 'NONE', #11255, 3.047499999999999876, 1.047197551196590748 ) ;
#9795=DIRECTION ( 'NONE',  ( -1.000000000000000000, -0.000000000000000000, -0.000000000000000000 ) ) ;
#9809=ORIENTED_EDGE ( 'NONE', *, *, #12833, .F. ) ;
#9833=ORIENTED_EDGE ( 'NONE', *, *, #2991, .T. ) ;
#9869=VECTOR ( 'NONE', #7252, 1000.000000000000000 ) ;
#9949=ORIENTED_EDGE ( 'NONE', *, *, #3443, .T. ) ;
#9953=VECTOR ( 'NONE', #8284, 1000.000000000000000 ) ;
#9956=CARTESIAN_POINT ( 'NONE',  ( 8.399999999999998579, 0.000000000000000000, 4.000000000000001776 ) ) ;
#9957=DIRECTION ( 'NONE',  ( -1.000000000000000000, -0.000000000000000000, -0.000000000000000000 ) ) ;
#9979=DIRECTION ( 'NONE',  ( -1.000000000000000000, -0.000000000000000000, -0.000000000000000000 ) ) ;
#10009=VERTEX_POINT ( 'NONE', #17866 ) ;
#10020=DIRECTION ( 'NONE',  ( -1.000000000000000000, -0.000000000000000000, -0.000000000000000000 ) ) ;
#10044=DIRECTION ( 'NONE',  ( 0.000000000000000000, 0.000000000000000000, 1.000000000000000000 ) ) ;
#10045=EDGE_CURVE ( 'NONE', #4093, #13916, #17687, .T. ) ;
#10094=PLANE ( 'NONE',  #3916 ) ;
#10149=FILL_AREA_STYLE_COLOUR ( '', #7752 ) ;
#10156=EDGE_CURVE ( 'NONE', #4808, #10864, #17994, .T. ) ;
#10157=ORIENTED_EDGE ( 'NONE', *, *, #12270, .T. ) ;
#10169=ORIENTED_EDGE ( 'NONE', *, *, #4750, .F. ) ;
#10207=EDGE_CURVE ( 'NONE', #13916, #5047, #13478, .T. ) ;
#10208=CARTESIAN_POINT ( 'NONE',  ( 4.000000000000000000, -1.759474945355381292, 3.047500000000002540 ) ) ;
#10213=CYLINDRICAL_SURFACE ( 'NONE', #14148, 4.000000000000001776 ) ;
#10339=CIRCLE ( 'NONE', #17173, 3.047499999999999876 ) ;
#10342=ORIENTED_EDGE ( 'NONE', *, *, #4624, .T. ) ;
#10361=ORIENTED_EDGE ( 'NONE', *, *, #6294, .F. ) ;
#10424=PRODUCT_DEFINITION_FORMATION_WITH_SPECIFIED_SOURCE ( 'ANY', '', #6792, .NOT_KNOWN. ) ;
#10434=CIRCLE ( 'NONE', #15485, 0.4000000000000001887 ) ;
#10435=SURFACE_STYLE_USAGE ( .BOTH. , #17233 ) ;
#10469=ORIENTED_EDGE ( 'NONE', *, *, #9374, .T. ) ;
#10520=CARTESIAN_POINT ( 'NONE',  ( -31.74999999999995737, 4.898587196589415787E-16, -4.000000000000001776 ) ) ;
#10608=DIRECTION ( 'NONE',  ( 0.000000000000000000, -1.000000000000000000, 9.859324684083080328E-16 ) ) ;
#10617=EDGE_LOOP ( 'NONE', ( #7204, #17790, #12589, #9809, #10469 ) ) ;
#10626=VERTEX_POINT ( 'NONE', #5025 ) ;
#10703=LINE ( 'NONE', #10520, #1233 ) ;
#10720=CARTESIAN_POINT ( 'NONE',  ( 4.000000000000000000, -1.759474945355381292, 3.047500000000002540 ) ) ;
#10727=AXIS2_PLACEMENT_3D ( 'NONE', #3403, #7466, #5982 ) ;
#10770=SHAPE_REPRESENTATION ( 'socket head cap screw_iso_ISO 4762 M8 x 12 - 12N', ( #16940 ), #3923 ) ;
#10792=EDGE_CURVE ( 'NONE', #11376, #14634, #516, .T. ) ;
#10797=DIRECTION ( 'NONE',  ( -1.000000000000000000, -0.000000000000000000, -0.000000000000000000 ) ) ;
#10800=EDGE_CURVE ( 'NONE', #3808, #6738, #4332, .T. ) ;
#10815=CARTESIAN_POINT ( 'NONE',  ( -31.74999999999995737, 0.000000000000000000, 0.000000000000000000 ) ) ;
#10838=CARTESIAN_POINT ( 'NONE',  ( 19.30950000000002120, 0.000000000000000000, 4.000000000000000888 ) ) ;
#10851=UNCERTAINTY_MEASURE_WITH_UNIT (LENGTH_MEASURE( 1.000000000000000082E-05 ), #8221, 'distance_accuracy_value', 'NONE');
#10864=VERTEX_POINT ( 'NONE', #13045 ) ;
#10902=LINE ( 'NONE', #16393, #17077 ) ;
#10912=DIRECTION ( 'NONE',  ( -1.000000000000000000, -0.000000000000000000, -0.000000000000000000 ) ) ;
#10919=CARTESIAN_POINT ( 'NONE',  ( 4.000000000000000000, 0.000000000000000000, 0.000000000000000000 ) ) ;
#10922=VERTEX_POINT ( 'NONE', #11739 ) ;
#10961=DIRECTION ( 'NONE',  ( -0.5000000000000061062, 1.060575238724902601E-16, -0.8660254037844351549 ) ) ;
#10979=CARTESIAN_POINT ( 'NONE',  ( 4.000000000000000000, 3.518949890710770134, -4.119968255444916849E-15 ) ) ;
#10999=EDGE_CURVE ( 'NONE', #7792, #6738, #3508, .T. ) ;
#11018=ADVANCED_FACE ( 'NONE', ( #3768 ), #1186, .T. ) ;
#11045=CARTESIAN_POINT ( 'NONE',  ( 4.000000000000000000, 3.518949890710770134, -4.119968255444916849E-15 ) ) ;
#11061=CIRCLE ( 'NONE', #1002, 3.309499999999999886 ) ;
#11068=EDGE_CURVE ( 'NONE', #10009, #1326, #13780, .T. ) ;
#11100=CARTESIAN_POINT ( 'NONE',  ( 4.000000000000000000, 3.518949890710770134, -4.119968255444916849E-15 ) ) ;
#11109=DIRECTION ( 'NONE',  ( -1.000000000000000000, -0.000000000000000000, -0.000000000000000000 ) ) ;
#11130=CARTESIAN_POINT ( 'NONE',  ( 4.000000000000000000, -3.518949890710769246, 4.119968255444916849E-15 ) ) ;
#11218=ADVANCED_FACE ( 'NONE', ( #17127 ), #16219, .T. ) ;
#11255=AXIS2_PLACEMENT_3D ( 'NONE', #6045, #7062, #7339 ) ;
#11258=CARTESIAN_POINT ( 'NONE',  ( 4.000000000000000000, 3.518949890710770134, -4.119968255444916849E-15 ) ) ;
#11279=DIRECTION ( 'NONE',  ( -1.000000000000000000, -0.000000000000000000, -0.000000000000000000 ) ) ;
#11297=CIRCLE ( 'NONE', #14011, 6.500000000000000000 ) ;
#11339=EDGE_CURVE ( 'NONE', #13916, #10922, #5546, .T. ) ;
#11375=ORIENTED_EDGE ( 'NONE', *, *, #17147, .T. ) ;
#11376=VERTEX_POINT ( 'NONE', #5709 ) ;
#11377=DIRECTION ( 'NONE',  ( 0.000000000000000000, 1.000000000000000000, -1.224646799147353207E-16 ) ) ;
#11424=DIRECTION ( 'NONE',  ( 0.000000000000000000, 0.000000000000000000, 1.000000000000000000 ) ) ;
#11425=DIRECTION ( 'NONE',  ( -1.000000000000000000, -0.000000000000000000, -0.000000000000000000 ) ) ;
#11445=SHAPE_REPRESENTATION_RELATIONSHIP ( 'NONE' , 'NONE' ,  #10770, #12694 ) ;
#11472=ORIENTED_EDGE ( 'NONE', *, *, #6294, .T. ) ;
#11485=LINE ( 'NONE', #14673, #6475 ) ;
#11500=CARTESIAN_POINT ( 'NONE',  ( 0.000000000000000000, 1.759474945355381514, -3.047500000000001652 ) ) ;
#11501=CIRCLE ( 'NONE', #14207, 4.000000000000000888 ) ;
#11580=DIRECTION ( 'NONE',  ( 0.000000000000000000, -0.5000000000000012212, -0.8660254037844380415 ) ) ;
#11615=CARTESIAN_POINT ( 'NONE',  ( 0.3999999999999975797, 0.000000000000000000, 0.000000000000000000 ) ) ;
#11617=EDGE_LOOP ( 'NONE', ( #4970, #7418, #14840 ) ) ;
#11618=AXIS2_PLACEMENT_3D ( 'NONE', #13975, #17993, #14060 ) ;
#11656=CARTESIAN_POINT ( 'NONE',  ( 4.000000000000000000, -3.004629197474318457E-15, -3.047499999999999876 ) ) ;
#11657=ORIENTED_EDGE ( 'NONE', *, *, #483, .F. ) ;
#11678=ADVANCED_FACE ( 'NONE', ( #9037 ), #7639, .T. ) ;
#11684=DIRECTION ( 'NONE',  ( 0.000000000000000000, 0.5000000000000012212, 0.8660254037844380415 ) ) ;
#11708=VECTOR ( 'NONE', #1753, 1000.000000000000114 ) ;
#11739=CARTESIAN_POINT ( 'NONE',  ( 4.000000000000000000, 2.639212418033077601, 1.523749999999997717 ) ) ;
#11764=DIRECTION ( 'NONE',  ( -0.7071067811865383579, 8.659560562355047490E-17, -0.7071067811865567876 ) ) ;
#11794=DIRECTION ( 'NONE',  ( -0.7071067811865383579, 0.000000000000000000, 0.7071067811865567876 ) ) ;
#11823=( LENGTH_UNIT ( ) NAMED_UNIT ( * ) SI_UNIT ( .MILLI., .METRE. ) );
#11882=EDGE_CURVE ( 'NONE', #10922, #5047, #9310, .T. ) ;
#11891=EDGE_LOOP ( 'NONE', ( #14598, #15319, #8296, #16978 ) ) ;
#11908=CARTESIAN_POINT ( 'NONE',  ( 0.000000000000000000, 1.759474945355381514, -3.047500000000001652 ) ) ;
#11909=DIRECTION ( 'NONE',  ( 0.000000000000000000, 0.000000000000000000, 1.000000000000000000 ) ) ;
#11944=CARTESIAN_POINT ( 'NONE',  ( 8.399999999999998579, 0.000000000000000000, 0.000000000000000000 ) ) ;
#11993=CARTESIAN_POINT ( 'NONE',  ( 4.000000000000000000, -1.759474945355381292, 3.047500000000002540 ) ) ;
#12017=DIRECTION ( 'NONE',  ( 1.000000000000000000, 0.000000000000000000, 0.000000000000000000 ) ) ;
#12026=EDGE_LOOP ( 'NONE', ( #374, #190, #17891, #9716, #17230 ) ) ;
#12058=AXIS2_PLACEMENT_3D ( 'NONE', #12655, #8389, #5792 ) ;
#12083=DIRECTION ( 'NONE',  ( 0.000000000000000000, 1.000000000000000000, -1.478898702612462246E-15 ) ) ;
#12092=VECTOR ( 'NONE', #3613, 1000.000000000000227 ) ;
#12107=CARTESIAN_POINT ( 'NONE',  ( 4.000000000000000000, 3.518949890710770134, -4.119968255444916849E-15 ) ) ;
#12222=DIRECTION ( 'NONE',  ( 1.000000000000000000, 0.000000000000000000, 0.000000000000000000 ) ) ;
#12223=TOROIDAL_SURFACE ( 'NONE', #17298, 6.099999999999999645, 0.4000000000000000222 ) ;
#12224=LINE ( 'NONE', #7779, #12092 ) ;
#12249=LINE ( 'NONE', #11045, #9484 ) ;
#12250=ADVANCED_FACE ( 'NONE', ( #1705 ), #17583, .F. ) ;
#12270=EDGE_CURVE ( 'NONE', #7005, #17537, #14164, .T. ) ;
#12311=CARTESIAN_POINT ( 'NONE',  ( 8.000000000000000000, 6.500000000000000000, 0.000000000000000000 ) ) ;
#12338=CARTESIAN_POINT ( 'NONE',  ( 4.000000000000000000, 1.759474945355381514, -3.047500000000001652 ) ) ;
#12397=CARTESIAN_POINT ( 'NONE',  ( -31.74999999999995737, 0.000000000000000000, 4.000000000000001776 ) ) ;
#12427=CIRCLE ( 'NONE', #302, 3.047499999999999876 ) ;
#12442=VERTEX_POINT ( 'NONE', #3463 ) ;
#12455=CARTESIAN_POINT ( 'NONE',  ( 20.00000000000000355, 4.475777889183788807E-16, -3.309499999999999886 ) ) ;
#12495=CARTESIAN_POINT ( 'NONE',  ( 19.30950000000002120, 0.000000000000000000, 0.000000000000000000 ) ) ;
#12508=ORIENTED_EDGE ( 'NONE', *, *, #9034, .T. ) ;
#12576=FACE_OUTER_BOUND ( 'NONE', #3, .T. ) ;
#12583=DIRECTION ( 'NONE',  ( 0.000000000000000000, 0.000000000000000000, -1.000000000000000000 ) ) ;
#12589=ORIENTED_EDGE ( 'NONE', *, *, #15002, .F. ) ;
#12593=DIRECTION ( 'NONE',  ( 1.000000000000000000, 0.000000000000000000, 0.000000000000000000 ) ) ;
#12594=( NAMED_UNIT ( * ) SI_UNIT ( $, .STERADIAN. ) SOLID_ANGLE_UNIT ( ) );
#12655=CARTESIAN_POINT ( 'NONE',  ( 20.00000000000000355, 0.000000000000000000, 0.000000000000000000 ) ) ;
#12694=ADVANCED_BREP_SHAPE_REPRESENTATION ( '', ( #1642, #16940 ), #3923 ) ;
#12724=FACE_OUTER_BOUND ( 'NONE', #9714, .T. ) ;
#12742=DIRECTION ( 'NONE',  ( -0.000000000000000000, 0.000000000000000000, 1.000000000000000000 ) ) ;
#12753=ORIENTED_EDGE ( 'NONE', *, *, #8583, .T. ) ;
#12762=EDGE_LOOP ( 'NONE', ( #7008, #12508, #13770, #18337 ) ) ;
#12801=CIRCLE ( 'NONE', #376, 4.000000000000001776 ) ;
#12833=EDGE_CURVE ( 'NONE', #15136, #526, #5757, .T. ) ;
#12844=ORIENTED_EDGE ( 'NONE', *, *, #3328, .T. ) ;
#12871=EDGE_CURVE ( 'NONE', #8755, #3130, #11485, .T. ) ;
#12903=DIRECTION ( 'NONE',  ( 0.000000000000000000, -1.000000000000000000, 1.478898702612462246E-15 ) ) ;
#12915=ORIENTED_EDGE ( 'NONE', *, *, #4619, .F. ) ;
#12940=EDGE_CURVE ( 'NONE', #3808, #13373, #7411, .T. ) ;
#12954=VERTEX_POINT ( 'NONE', #10838 ) ;
#12955=EDGE_LOOP ( 'NONE', ( #17275, #3557, #4850 ) ) ;
#12968=CARTESIAN_POINT ( 'NONE',  ( 8.000000000000000000, 0.000000000000000000, 6.500000000000000000 ) ) ;
#12991=LINE ( 'NONE', #7057, #4024 ) ;
#12992=ADVANCED_FACE ( 'NONE', ( #9179 ), #15967, .T. ) ;
#12993=VECTOR ( 'NONE', #13413, 999.9999999999998863 ) ;
#13045=CARTESIAN_POINT ( 'NONE',  ( 0.000000000000000000, 7.715274834628324392E-16, -6.099999999999999645 ) ) ;
#13070=DIRECTION ( 'NONE',  ( 0.000000000000000000, -1.000000000000000000, 9.859324684083080328E-16 ) ) ;
#13074=FACE_OUTER_BOUND ( 'NONE', #552, .T. ) ;
#13093=DIRECTION ( 'NONE',  ( 0.000000000000000000, 0.000000000000000000, 1.000000000000000000 ) ) ;
#13195=CIRCLE ( 'NONE', #8750, 6.500000000000000000 ) ;
#13248=CARTESIAN_POINT ( 'NONE',  ( 0.3999999999999975797, 0.000000000000000000, 6.099999999999999645 ) ) ;
#13284=DIRECTION ( 'NONE',  ( -1.000000000000000000, -0.000000000000000000, -0.000000000000000000 ) ) ;
#13287=CARTESIAN_POINT ( 'NONE',  ( 0.3999999999999975797, 0.000000000000000000, 6.500000000000000000 ) ) ;
#13295=DIRECTION ( 'NONE',  ( 0.000000000000000000, 0.4999999999999992784, -0.8660254037844389297 ) ) ;
#13373=VERTEX_POINT ( 'NONE', #11656 ) ;
#13375=CARTESIAN_POINT ( 'NONE',  ( 19.30950000000002120, 0.000000000000000000, 0.000000000000000000 ) ) ;
#13402=FACE_OUTER_BOUND ( 'NONE', #16542, .T. ) ;
#13413=DIRECTION ( 'NONE',  ( 0.000000000000000000, -0.5000000000000012212, -0.8660254037844380415 ) ) ;
#13437=DIRECTION ( 'NONE',  ( -1.000000000000000000, -0.000000000000000000, -0.000000000000000000 ) ) ;
#13478=LINE ( 'NONE', #11993, #9953 ) ;
#13484=CARTESIAN_POINT ( 'NONE',  ( 4.000000000000000000, 2.639212418033075380, -1.523750000000004157 ) ) ;
#13488=PLANE ( 'NONE',  #10727 ) ;
#13501=CARTESIAN_POINT ( 'NONE',  ( 0.000000000000000000, -3.518949890710769246, 4.119968255444916849E-15 ) ) ;
#13549=ORIENTED_EDGE ( 'NONE', *, *, #5595, .T. ) ;
#13557=DIRECTION ( 'NONE',  ( 0.000000000000000000, 0.000000000000000000, 1.000000000000000000 ) ) ;
#13593=CARTESIAN_POINT ( 'NONE',  ( 8.399999999999998579, 0.000000000000000000, 0.000000000000000000 ) ) ;
#13598=CARTESIAN_POINT ( 'NONE',  ( -31.74999999999995737, 7.960204194457795477E-16, -6.500000000000000000 ) ) ;
#13628=VERTEX_POINT ( 'NONE', #12455 ) ;
#13672=AXIS2_PLACEMENT_3D ( 'NONE', #3348, #752, #8994 ) ;
#13702=LINE ( 'NONE', #16598, #9562 ) ;
#13709=CARTESIAN_POINT ( 'NONE',  ( 4.000000000000000000, -3.518949890710769246, 4.119968255444916849E-15 ) ) ;
#13717=DIRECTION ( 'NONE',  ( 0.000000000000000000, 0.000000000000000000, 1.000000000000000000 ) ) ;
#13770=ORIENTED_EDGE ( 'NONE', *, *, #6706, .T. ) ;
#13780=LINE ( 'NONE', #13501, #17106 ) ;
#13829=CARTESIAN_POINT ( 'NONE',  ( 8.000000000000000000, 0.000000000000000000, 0.000000000000000000 ) ) ;
#13866=ADVANCED_FACE ( 'NONE', ( #5955 ), #10213, .T. ) ;
#13885=( NAMED_UNIT ( * ) PLANE_ANGLE_UNIT ( ) SI_UNIT ( $, .RADIAN. ) );
#13894=CARTESIAN_POINT ( 'NONE',  ( 0.000000000000000000, 0.000000000000000000, 0.000000000000000000 ) ) ;
#13916=VERTEX_POINT ( 'NONE', #9114 ) ;
#13919=AXIS2_PLACEMENT_3D ( 'NONE', #13894, #1205, #13983 ) ;
#13964=VERTEX_POINT ( 'NONE', #13287 ) ;
#13975=CARTESIAN_POINT ( 'NONE',  ( 4.000000000000000000, 3.518949890710770134, -4.119968255444916849E-15 ) ) ;
#13983=DIRECTION ( 'NONE',  ( 0.000000000000000000, 0.000000000000000000, 1.000000000000000000 ) ) ;
#13999=CIRCLE ( 'NONE', #391, 3.047499999999999876 ) ;
#14011=AXIS2_PLACEMENT_3D ( 'NONE', #2520, #12593, #18107 ) ;
#14041=DIRECTION ( 'NONE',  ( 0.000000000000000000, 0.8660254037844380415, -0.5000000000000012212 ) ) ;
#14060=DIRECTION ( 'NONE',  ( 0.000000000000000000, 0.000000000000000000, -1.000000000000000000 ) ) ;
#14099=TOROIDAL_SURFACE ( 'NONE', #3739, 4.400000000000002132, 0.4000000000000000222 ) ;
#14137=VECTOR ( 'NONE', #9154, 999.9999999999998863 ) ;
#14141=CARTESIAN_POINT ( 'NONE',  ( 4.000000000000000000, -2.639212418033074492, 1.523750000000003046 ) ) ;
#14148=AXIS2_PLACEMENT_3D ( 'NONE', #599, #3469, #8729 ) ;
#14164=CIRCLE ( 'NONE', #4092, 6.500000000000000000 ) ;
#14207=AXIS2_PLACEMENT_3D ( 'NONE', #12495, #3885, #18189 ) ;
#14238=CARTESIAN_POINT ( 'NONE',  ( 19.30950000000002120, 4.898587196589414801E-16, -4.000000000000000888 ) ) ;
#14310=FACE_OUTER_BOUND ( 'NONE', #12026, .T. ) ;
#14317=EDGE_LOOP ( 'NONE', ( #8919, #2538, #11375, #7248, #13549 ) ) ;
#14322=CARTESIAN_POINT ( 'NONE',  ( 4.000000000000000000, -1.759474945355381292, 3.047500000000002540 ) ) ;
#14341=( NAMED_UNIT ( * ) SI_UNIT ( $, .STERADIAN. ) SOLID_ANGLE_UNIT ( ) );
#14353=DIRECTION ( 'NONE',  ( -1.000000000000000000, -0.000000000000000000, -0.000000000000000000 ) ) ;
#14411=EDGE_CURVE ( 'NONE', #10626, #12954, #411, .T. ) ;
#14422=EDGE_CURVE ( 'NONE', #16136, #12954, #17143, .T. ) ;
#14452=VECTOR ( 'NONE', #7824, 1000.000000000000227 ) ;
#14479=AXIS2_PLACEMENT_3D ( 'NONE', #13375, #13284, #1804 ) ;
#14480=DIRECTION ( 'NONE',  ( 0.000000000000000000, 0.4999999999999990008, -0.8660254037844391517 ) ) ;
#14496=CARTESIAN_POINT ( 'NONE',  ( -31.74999999999995737, 0.000000000000000000, 0.000000000000000000 ) ) ;
#14503=DIRECTION ( 'NONE',  ( 0.000000000000000000, 0.000000000000000000, 1.000000000000000000 ) ) ;
#14504=DIRECTION ( 'NONE',  ( -0.000000000000000000, 1.478898702612462246E-15, 1.000000000000000000 ) ) ;
#14547=CARTESIAN_POINT ( 'NONE',  ( 0.000000000000000000, 3.518949890710770134, -4.119968255444916849E-15 ) ) ;
#14586=EDGE_CURVE ( 'NONE', #7792, #4253, #12224, .T. ) ;
#14598=ORIENTED_EDGE ( 'NONE', *, *, #8583, .F. ) ;
#14624=AXIS2_PLACEMENT_3D ( 'NONE', #5533, #9795, #17137 ) ;
#14634=VERTEX_POINT ( 'NONE', #9533 ) ;
#14654=DIRECTION ( 'NONE',  ( 1.000000000000000000, 0.000000000000000000, 0.000000000000000000 ) ) ;
#14673=CARTESIAN_POINT ( 'NONE',  ( 4.000000000000000000, -3.518949890710769246, 4.119968255444916849E-15 ) ) ;
#14695=ORIENTED_EDGE ( 'NONE', *, *, #7940, .F. ) ;
#14705=PLANE ( 'NONE',  #18200 ) ;
#14719=ORIENTED_EDGE ( 'NONE', *, *, #8982, .F. ) ;
#14733=DIRECTION ( 'NONE',  ( 1.000000000000000000, 0.000000000000000000, 0.000000000000000000 ) ) ;
#14743=ORIENTED_EDGE ( 'NONE', *, *, #16967, .T. ) ;
#14793=ORIENTED_EDGE ( 'NONE', *, *, #12871, .F. ) ;
#14824=CIRCLE ( 'NONE', #13919, 6.099999999999999645 ) ;
#14837=AXIS2_PLACEMENT_3D ( 'NONE', #5772, #32, #14503 ) ;
#14840=ORIENTED_EDGE ( 'NONE', *, *, #11339, .F. ) ;
#14937=PRODUCT_CONTEXT ( 'NONE', #7236, 'mechanical' ) ;
#14992=DIRECTION ( 'NONE',  ( -1.000000000000000000, -0.000000000000000000, -0.000000000000000000 ) ) ;
#15002=EDGE_CURVE ( 'NONE', #526, #3808, #7754, .T. ) ;
#15067=ADVANCED_FACE ( 'NONE', ( #17803 ), #5064, .T. ) ;
#15088=ORIENTED_EDGE ( 'NONE', *, *, #4624, .F. ) ;
#15092=VECTOR ( 'NONE', #13437, 1000.000000000000000 ) ;
#15114=ADVANCED_FACE ( 'NONE', ( #16122 ), #3413, .F. ) ;
#15136=VERTEX_POINT ( 'NONE', #11258 ) ;
#15211=FACE_BOUND ( 'NONE', #1773, .T. ) ;
#15237=AXIS2_PLACEMENT_3D ( 'NONE', #7074, #5872, #8463 ) ;
#15296=AXIS2_PLACEMENT_3D ( 'NONE', #17213, #130, #12742 ) ;
#15299=CARTESIAN_POINT ( 'NONE',  ( 8.399999999999998579, 4.898587196589415787E-16, -4.000000000000001776 ) ) ;
#15319=ORIENTED_EDGE ( 'NONE', *, *, #5115, .T. ) ;
#15336=AXIS2_PLACEMENT_3D ( 'NONE', #10815, #2579, #6462 ) ;
#15391=FACE_OUTER_BOUND ( 'NONE', #1643, .T. ) ;
#15478=ORIENTED_EDGE ( 'NONE', *, *, #18139, .F. ) ;
#15485=AXIS2_PLACEMENT_3D ( 'NONE', #270, #11377, #4435 ) ;
#15553=ORIENTED_EDGE ( 'NONE', *, *, #10792, .T. ) ;
#15675=CIRCLE ( 'NONE', #7666, 3.047499999999999876 ) ;
#15696=AXIS2_PLACEMENT_3D ( 'NONE', #2857, #4514, #12583 ) ;
#15701=DIRECTION ( 'NONE',  ( -1.000000000000000000, -0.000000000000000000, -0.000000000000000000 ) ) ;
#15762=ORIENTED_EDGE ( 'NONE', *, *, #10207, .F. ) ;
#15763=VECTOR ( 'NONE', #4987, 1000.000000000000000 ) ;
#15795=UNCERTAINTY_MEASURE_WITH_UNIT (LENGTH_MEASURE( 1.000000000000000082E-05 ), #11823, 'distance_accuracy_value', 'NONE');
#15825=ORIENTED_EDGE ( 'NONE', *, *, #10792, .F. ) ;
#15827=CARTESIAN_POINT ( 'NONE',  ( 4.000000000000000000, 1.759474945355381514, -3.047500000000001652 ) ) ;
#15831=VERTEX_POINT ( 'NONE', #14141 ) ;
#15923=AXIS2_PLACEMENT_3D ( 'NONE', #6993, #9957, #7086 ) ;
#15967=CONICAL_SURFACE ( 'NONE', #7306, 3.309499999999999886, 0.7853981633974613796 ) ;
#15974=CARTESIAN_POINT ( 'NONE',  ( 0.000000000000000000, 1.759474945355387954, 3.047499999999997211 ) ) ;
#16017=PRESENTATION_STYLE_ASSIGNMENT (( #10435 ) ) ;
#16022=ORIENTED_EDGE ( 'NONE', *, *, #3092, .T. ) ;
#16026=ORIENTED_EDGE ( 'NONE', *, *, #8982, .T. ) ;
#16052=VERTEX_POINT ( 'NONE', #9956 ) ;
#16063=CARTESIAN_POINT ( 'NONE',  ( 4.000000000000000000, 1.759474945355381514, -3.047500000000001652 ) ) ;
#16095=FACE_OUTER_BOUND ( 'NONE', #14317, .T. ) ;
#16114=DIRECTION ( 'NONE',  ( -1.000000000000000000, -0.000000000000000000, -0.000000000000000000 ) ) ;
#16122=FACE_OUTER_BOUND ( 'NONE', #12955, .T. ) ;
#16123=EDGE_CURVE ( 'NONE', #13373, #8755, #12427, .T. ) ;
#16136=VERTEX_POINT ( 'NONE', #14238 ) ;
#16153=DIRECTION ( 'NONE',  ( 0.000000000000000000, 0.000000000000000000, 1.000000000000000000 ) ) ;
#16209=EDGE_CURVE ( 'NONE', #6738, #1326, #6255, .T. ) ;
#16219=CONICAL_SURFACE ( 'NONE', #12058, 3.309499999999999886, 0.7853981633974613796 ) ;
#16271=ORIENTED_EDGE ( 'NONE', *, *, #16209, .T. ) ;
#16277=CARTESIAN_POINT ( 'NONE',  ( 4.000000000000000000, 3.518949890710770134, -4.119968255444916849E-15 ) ) ;
#16314=ORIENTED_EDGE ( 'NONE', *, *, #11068, .F. ) ;
#16393=CARTESIAN_POINT ( 'NONE',  ( 4.000000000000000000, 1.759474945355381514, -3.047500000000001652 ) ) ;
#16419=VECTOR ( 'NONE', #11764, 999.9999999999998863 ) ;
#16484=AXIS2_PLACEMENT_3D ( 'NONE', #9473, #3821, #9569 ) ;
#16516=ORIENTED_EDGE ( 'NONE', *, *, #12270, .F. ) ;
#16540=FACE_OUTER_BOUND ( 'NONE', #5899, .T. ) ;
#16542=EDGE_LOOP ( 'NONE', ( #1291, #393 ) ) ;
#16543=AXIS2_PLACEMENT_3D ( 'NONE', #617, #6256, #11909 ) ;
#16571=CARTESIAN_POINT ( 'NONE',  ( 20.00000000000000355, 0.000000000000000000, 0.000000000000000000 ) ) ;
#16585=EDGE_CURVE ( 'NONE', #13964, #4808, #1195, .T. ) ;
#16598=CARTESIAN_POINT ( 'NONE',  ( 4.000000000000000000, -3.518949890710769246, 4.119968255444916849E-15 ) ) ;
#16601=ORIENTED_EDGE ( 'NONE', *, *, #7094, .F. ) ;
#16665=PLANE ( 'NONE',  #3046 ) ;
#16694=CIRCLE ( 'NONE', #2763, 3.309499999999999886 ) ;
#16757=ADVANCED_FACE ( 'NONE', ( #14310 ), #9778, .F. ) ;
#16780=AXIS2_PLACEMENT_3D ( 'NONE', #6872, #7047, #18036 ) ;
#16857=VECTOR ( 'NONE', #11794, 999.9999999999998863 ) ;
#16917=VECTOR ( 'NONE', #17581, 1000.000000000000000 ) ;
#16940=AXIS2_PLACEMENT_3D ( 'NONE', #9024, #13557, #6428 ) ;
#16967=EDGE_CURVE ( 'NONE', #7588, #4253, #3643, .T. ) ;
#16978=ORIENTED_EDGE ( 'NONE', *, *, #14422, .F. ) ;
#17001=ADVANCED_FACE ( 'NONE', ( #16540 ), #1323, .T. ) ;
#17006=DIRECTION ( 'NONE',  ( 1.000000000000000000, 0.000000000000000000, 0.000000000000000000 ) ) ;
#17017=VECTOR ( 'NONE', #17402, 1000.000000000000000 ) ;
#17077=VECTOR ( 'NONE', #5340, 1000.000000000000000 ) ;
#17092=ORIENTED_EDGE ( 'NONE', *, *, #14422, .T. ) ;
#17106=VECTOR ( 'NONE', #7938, 1000.000000000000227 ) ;
#17127=FACE_OUTER_BOUND ( 'NONE', #7619, .T. ) ;
#17137=DIRECTION ( 'NONE',  ( 0.000000000000000000, 0.000000000000000000, 1.000000000000000000 ) ) ;
#17143=CIRCLE ( 'NONE', #14479, 4.000000000000000888 ) ;
#17147=EDGE_CURVE ( 'NONE', #15136, #10922, #12249, .T. ) ;
#17158=ORIENTED_EDGE ( 'NONE', *, *, #8626, .F. ) ;
#17173=AXIS2_PLACEMENT_3D ( 'NONE', #3936, #9586, #5419 ) ;
#17213=CARTESIAN_POINT ( 'NONE',  ( 0.000000000000000000, 0.000000000000000000, 0.000000000000000000 ) ) ;
#17214=ORIENTED_EDGE ( 'NONE', *, *, #6265, .F. ) ;
#17230=ORIENTED_EDGE ( 'NONE', *, *, #664, .T. ) ;
#17233=SURFACE_SIDE_STYLE ('',( #8951 ) ) ;
#17254=ORIENTED_EDGE ( 'NONE', *, *, #483, .T. ) ;
#17275=ORIENTED_EDGE ( 'NONE', *, *, #17147, .F. ) ;
#17283=EDGE_LOOP ( 'NONE', ( #14743, #6541, #15762, #7168, #1976 ) ) ;
#17298=AXIS2_PLACEMENT_3D ( 'NONE', #759, #6219, #17656 ) ;
#17310=CARTESIAN_POINT ( 'NONE',  ( 4.000000000000000000, 3.518949890710770134, -4.119968255444916849E-15 ) ) ;
#17311=PLANE ( 'NONE',  #15296 ) ;
#17351=EDGE_LOOP ( 'NONE', ( #3692, #2352, #708, #17214 ) ) ;
#17374=EDGE_LOOP ( 'NONE', ( #11657, #6469, #2944 ) ) ;
#17388=EDGE_CURVE ( 'NONE', #17537, #4808, #9157, .T. ) ;
#17402=DIRECTION ( 'NONE',  ( -1.000000000000000000, -0.000000000000000000, -0.000000000000000000 ) ) ;
#17423=DIRECTION ( 'NONE',  ( 0.000000000000000000, 0.000000000000000000, 1.000000000000000000 ) ) ;
#17537=VERTEX_POINT ( 'NONE', #2308 ) ;
#17581=DIRECTION ( 'NONE',  ( 0.000000000000000000, 1.000000000000000000, -1.478898702612462246E-15 ) ) ;
#17583=PLANE ( 'NONE',  #2629 ) ;
#17656=DIRECTION ( 'NONE',  ( 0.000000000000000000, 0.000000000000000000, 1.000000000000000000 ) ) ;
#17687=LINE ( 'NONE', #6623, #1678 ) ;
#17697=ORIENTED_EDGE ( 'NONE', *, *, #16123, .F. ) ;
#17715=ORIENTED_EDGE ( 'NONE', *, *, #10156, .T. ) ;
#17726=ORIENTED_EDGE ( 'NONE', *, *, #14411, .F. ) ;
#17790=ORIENTED_EDGE ( 'NONE', *, *, #10800, .F. ) ;
#17803=FACE_OUTER_BOUND ( 'NONE', #8956, .T. ) ;
#17857=VECTOR ( 'NONE', #6671, 1000.000000000000114 ) ;
#17866=CARTESIAN_POINT ( 'NONE',  ( 0.000000000000000000, -3.518949890710769246, 4.119968255444916849E-15 ) ) ;
#17887=FACE_OUTER_BOUND ( 'NONE', #7742, .T. ) ;
#17891=ORIENTED_EDGE ( 'NONE', *, *, #16123, .T. ) ;
#17904=TOROIDAL_SURFACE ( 'NONE', #2201, 6.099999999999999645, 0.4000000000000000222 ) ;
#17905=EDGE_LOOP ( 'NONE', ( #16271, #5211, #14695, #7863, #250 ) ) ;
#17909=LINE ( 'NONE', #13709, #6202 ) ;
#17960=CIRCLE ( 'NONE', #16484, 4.400000000000002132 ) ;
#17993=DIRECTION ( 'NONE',  ( 1.000000000000000000, 0.000000000000000000, 0.000000000000000000 ) ) ;
#17994=CIRCLE ( 'NONE', #1102, 0.4000000000000001887 ) ;
#18027=CLOSED_SHELL ( 'NONE', ( #16757, #5476, #9554, #11218, #11018, #6713, #9370, #11678, #7391, #13866, #12992, #3953, #5416, #2317, #5691, #12250, #15067, #17001, #2322, #4185, #5578, #7521, #7363, #2749, #15114, #4674, #4789 ) ) ;
#18036=DIRECTION ( 'NONE',  ( 0.000000000000000000, 0.000000000000000000, -1.000000000000000000 ) ) ;
#18107=DIRECTION ( 'NONE',  ( 0.000000000000000000, 0.000000000000000000, 1.000000000000000000 ) ) ;
#18139=EDGE_CURVE ( 'NONE', #16136, #7494, #10703, .T. ) ;
#18147=CIRCLE ( 'NONE', #5966, 3.047499999999999876 ) ;
#18157=EDGE_LOOP ( 'NONE', ( #5692, #2233, #3562 ) ) ;
#18168=EDGE_LOOP ( 'NONE', ( #4739, #14793, #17697 ) ) ;
#18177=PLANE ( 'NONE',  #11618 ) ;
#18189=DIRECTION ( 'NONE',  ( 0.000000000000000000, 0.000000000000000000, 1.000000000000000000 ) ) ;
#18198=CARTESIAN_POINT ( 'NONE',  ( 4.000000000000000000, 0.000000000000000000, 0.000000000000000000 ) ) ;
#18200=AXIS2_PLACEMENT_3D ( 'NONE', #17310, #699, #3195 ) ;
#18300=DIRECTION ( 'NONE',  ( -0.000000000000000000, 0.8660254037844391517, 0.4999999999999990563 ) ) ;
#18337=ORIENTED_EDGE ( 'NONE', *, *, #16585, .T. ) ;
#18367=CARTESIAN_POINT ( 'NONE',  ( 8.000000000000000000, 0.000000000000000000, 0.000000000000000000 ) ) ;
#18411=COLOUR_RGB('Black',0.12,0.14,0.17);
#18412=FILL_AREA_STYLE_COLOUR('',#18411);
#18413=FILL_AREA_STYLE('',(#18412));
#18414=SURFACE_STYLE_FILL_AREA(#18413);
#18415=SURFACE_SIDE_STYLE('',(#18414));
#18416=SURFACE_STYLE_USAGE(.BOTH.,#18415);
#18417=PRESENTATION_STYLE_ASSIGNMENT((#18416));
ENDSEC;
END-ISO-10303-21;
